ISO-10303-21;
HEADER;
/* Generated by software containing ST-Developer
 * from STEP Tools, Inc. (www.steptools.com) 
 */

FILE_DESCRIPTION(
/* description */ ('Pedal-braked fixed caster'),
/* implementation_level */ '2;1');

FILE_NAME(
/* name */ 'Hex Nut - M6.step',
/* time_stamp */ '2026-10-28T03:26:52-07:00',
/* author */ (''),
/* organization */ (''),
/* preprocessor_version */ 'ST-DEVELOPER v20.2',
/* originating_system */ 'Autodesk Translation Framework v15.17.0.0',
/* authorisation */ '');

FILE_SCHEMA (('AUTOMOTIVE_DESIGN { 1 0 10303 214 3 1 1 }'));
ENDSEC;

DATA;
#10=MECHANICAL_DESIGN_GEOMETRIC_PRESENTATION_REPRESENTATION('',(#213),#5734);
#147=(
BOUNDED_CURVE()
B_SPLINE_CURVE(2,(#4934,#4935,#4936),.UNSPECIFIED.,.F.,.F.)
B_SPLINE_CURVE_WITH_KNOTS((3,3),(0.144988513094728,0.791574906712449),
 .UNSPECIFIED.)
CURVE()
GEOMETRIC_REPRESENTATION_ITEM()
RATIONAL_B_SPLINE_CURVE((1.09282032302755,1.26188021535082,1.09282032302931))
REPRESENTATION_ITEM('')
);
#148=(
BOUNDED_CURVE()
B_SPLINE_CURVE(2,(#4938,#4939,#4940),.UNSPECIFIED.,.F.,.F.)
B_SPLINE_CURVE_WITH_KNOTS((3,3),(0.144988513094728,0.791574906712449),
 .UNSPECIFIED.)
CURVE()
GEOMETRIC_REPRESENTATION_ITEM()
RATIONAL_B_SPLINE_CURVE((1.09282032302755,1.26188021535082,1.09282032302931))
REPRESENTATION_ITEM('')
);
#149=(
BOUNDED_CURVE()
B_SPLINE_CURVE(2,(#4945,#4946,#4947),.UNSPECIFIED.,.F.,.F.)
B_SPLINE_CURVE_WITH_KNOTS((3,3),(0.144988513094728,0.791574906712449),
 .UNSPECIFIED.)
CURVE()
GEOMETRIC_REPRESENTATION_ITEM()
RATIONAL_B_SPLINE_CURVE((1.09282032302755,1.26188021535082,1.09282032302931))
REPRESENTATION_ITEM('')
);
#150=(
BOUNDED_CURVE()
B_SPLINE_CURVE(2,(#4949,#4950,#4951),.UNSPECIFIED.,.F.,.F.)
B_SPLINE_CURVE_WITH_KNOTS((3,3),(0.144988513094728,0.791574906712449),
 .UNSPECIFIED.)
CURVE()
GEOMETRIC_REPRESENTATION_ITEM()
RATIONAL_B_SPLINE_CURVE((1.09282032302755,1.26188021535082,1.09282032302931))
REPRESENTATION_ITEM('')
);
#151=(
BOUNDED_CURVE()
B_SPLINE_CURVE(2,(#4953,#4954,#4955),.UNSPECIFIED.,.F.,.F.)
B_SPLINE_CURVE_WITH_KNOTS((3,3),(0.144988513094728,0.791574906712449),
 .UNSPECIFIED.)
CURVE()
GEOMETRIC_REPRESENTATION_ITEM()
RATIONAL_B_SPLINE_CURVE((1.09282032302755,1.26188021535082,1.09282032302931))
REPRESENTATION_ITEM('')
);
#152=(
BOUNDED_CURVE()
B_SPLINE_CURVE(2,(#4956,#4957,#4958),.UNSPECIFIED.,.F.,.F.)
B_SPLINE_CURVE_WITH_KNOTS((3,3),(0.144988513094728,0.791574906712449),
 .UNSPECIFIED.)
CURVE()
GEOMETRIC_REPRESENTATION_ITEM()
RATIONAL_B_SPLINE_CURVE((1.09282032302755,1.26188021535082,1.09282032302931))
REPRESENTATION_ITEM('')
);
#153=(
BOUNDED_CURVE()
B_SPLINE_CURVE(2,(#4965,#4966,#4967),.UNSPECIFIED.,.F.,.F.)
B_SPLINE_CURVE_WITH_KNOTS((3,3),(0.144988513094728,0.791574906712449),
 .UNSPECIFIED.)
CURVE()
GEOMETRIC_REPRESENTATION_ITEM()
RATIONAL_B_SPLINE_CURVE((1.09282032302755,1.26188021535082,1.09282032302931))
REPRESENTATION_ITEM('')
);
#154=(
BOUNDED_CURVE()
B_SPLINE_CURVE(2,(#4969,#4970,#4971),.UNSPECIFIED.,.F.,.F.)
B_SPLINE_CURVE_WITH_KNOTS((3,3),(0.144988513094727,0.791574906712449),
 .UNSPECIFIED.)
CURVE()
GEOMETRIC_REPRESENTATION_ITEM()
RATIONAL_B_SPLINE_CURVE((1.09282032302755,1.26188021535082,1.09282032302931))
REPRESENTATION_ITEM('')
);
#155=(
BOUNDED_CURVE()
B_SPLINE_CURVE(2,(#4973,#4974,#4975),.UNSPECIFIED.,.F.,.F.)
B_SPLINE_CURVE_WITH_KNOTS((3,3),(0.144988513094728,0.791574906712449),
 .UNSPECIFIED.)
CURVE()
GEOMETRIC_REPRESENTATION_ITEM()
RATIONAL_B_SPLINE_CURVE((1.09282032302755,1.26188021535082,1.09282032302931))
REPRESENTATION_ITEM('')
);
#156=(
BOUNDED_CURVE()
B_SPLINE_CURVE(2,(#4977,#4978,#4979),.UNSPECIFIED.,.F.,.F.)
B_SPLINE_CURVE_WITH_KNOTS((3,3),(0.144988513094728,0.791574906712449),
 .UNSPECIFIED.)
CURVE()
GEOMETRIC_REPRESENTATION_ITEM()
RATIONAL_B_SPLINE_CURVE((1.09282032302755,1.26188021535082,1.09282032302931))
REPRESENTATION_ITEM('')
);
#157=(
BOUNDED_CURVE()
B_SPLINE_CURVE(2,(#4981,#4982,#4983),.UNSPECIFIED.,.F.,.F.)
B_SPLINE_CURVE_WITH_KNOTS((3,3),(0.144988513094728,0.791574906712449),
 .UNSPECIFIED.)
CURVE()
GEOMETRIC_REPRESENTATION_ITEM()
RATIONAL_B_SPLINE_CURVE((1.09282032302755,1.26188021535082,1.09282032302931))
REPRESENTATION_ITEM('')
);
#158=(
BOUNDED_CURVE()
B_SPLINE_CURVE(2,(#4984,#4985,#4986),.UNSPECIFIED.,.F.,.F.)
B_SPLINE_CURVE_WITH_KNOTS((3,3),(0.144988513094727,0.791574906712449),
 .UNSPECIFIED.)
CURVE()
GEOMETRIC_REPRESENTATION_ITEM()
RATIONAL_B_SPLINE_CURVE((1.09282032302755,1.26188021535082,1.09282032302931))
REPRESENTATION_ITEM('')
);
#164=CONICAL_SURFACE('',#3344,0.576175134594813,1.0471975511966);
#165=CONICAL_SURFACE('',#3346,0.576175134594813,1.0471975511966);
#179=SHAPE_REPRESENTATION_RELATIONSHIP('SRR','None',#5817,#196);
#196=ADVANCED_BREP_SHAPE_REPRESENTATION('',(#236),#5721);
#213=STYLED_ITEM('',(#5991),#236);
#236=MANIFOLD_SOLID_BREP('Body1',#2995);
#273=CYLINDRICAL_SURFACE('',#3351,0.25175);
#321=FACE_BOUND('',#779,.T.);
#322=FACE_BOUND('',#781,.T.);
#385=CIRCLE('',#3345,0.475);
#386=CIRCLE('',#3347,0.475);
#387=CIRCLE('',#3352,0.25175);
#388=CIRCLE('',#3353,0.25175);
#565=FACE_OUTER_BOUND('',#769,.T.);
#566=FACE_OUTER_BOUND('',#770,.T.);
#567=FACE_OUTER_BOUND('',#771,.T.);
#568=FACE_OUTER_BOUND('',#772,.T.);
#569=FACE_OUTER_BOUND('',#773,.T.);
#570=FACE_OUTER_BOUND('',#774,.T.);
#571=FACE_OUTER_BOUND('',#775,.T.);
#572=FACE_OUTER_BOUND('',#776,.T.);
#573=FACE_OUTER_BOUND('',#777,.T.);
#574=FACE_OUTER_BOUND('',#778,.T.);
#575=FACE_OUTER_BOUND('',#780,.T.);
#769=EDGE_LOOP('',(#2332,#2333,#2334,#2335,#2336,#2337,#2338,#2339,#2340));
#770=EDGE_LOOP('',(#2341,#2342,#2343,#2344,#2345,#2346,#2347,#2348,#2349));
#771=EDGE_LOOP('',(#2350,#2351,#2352,#2353));
#772=EDGE_LOOP('',(#2354,#2355,#2356,#2357));
#773=EDGE_LOOP('',(#2358,#2359,#2360,#2361));
#774=EDGE_LOOP('',(#2362,#2363,#2364,#2365));
#775=EDGE_LOOP('',(#2366,#2367,#2368,#2369));
#776=EDGE_LOOP('',(#2370,#2371,#2372,#2373));
#777=EDGE_LOOP('',(#2374,#2375,#2376,#2377));
#778=EDGE_LOOP('',(#2378));
#779=EDGE_LOOP('',(#2379));
#780=EDGE_LOOP('',(#2380));
#781=EDGE_LOOP('',(#2381));
#1022=LINE('',#4942,#1234);
#1023=LINE('',#4963,#1235);
#1024=LINE('',#4988,#1236);
#1025=LINE('',#4989,#1237);
#1026=LINE('',#4991,#1238);
#1027=LINE('',#4993,#1239);
#1028=LINE('',#4998,#1240);
#1029=LINE('',#5001,#1241);
#1030=LINE('',#5003,#1242);
#1234=VECTOR('',#3996,0.576175134594813);
#1235=VECTOR('',#4003,0.576175134594813);
#1236=VECTOR('',#4006,1.);
#1237=VECTOR('',#4007,1.);
#1238=VECTOR('',#4010,1.);
#1239=VECTOR('',#4013,1.);
#1240=VECTOR('',#4018,0.3);
#1241=VECTOR('',#4023,1.);
#1242=VECTOR('',#4026,1.);
#1430=VERTEX_POINT('',#4932);
#1431=VERTEX_POINT('',#4933);
#1432=VERTEX_POINT('',#4937);
#1433=VERTEX_POINT('',#4941);
#1434=VERTEX_POINT('',#4944);
#1435=VERTEX_POINT('',#4948);
#1436=VERTEX_POINT('',#4952);
#1437=VERTEX_POINT('',#4960);
#1438=VERTEX_POINT('',#4962);
#1439=VERTEX_POINT('',#4964);
#1440=VERTEX_POINT('',#4968);
#1441=VERTEX_POINT('',#4972);
#1442=VERTEX_POINT('',#4976);
#1443=VERTEX_POINT('',#4980);
#1444=VERTEX_POINT('',#4995);
#1445=VERTEX_POINT('',#4997);
#1756=EDGE_CURVE('',#1430,#1431,#147,.T.);
#1757=EDGE_CURVE('',#1432,#1430,#148,.T.);
#1758=EDGE_CURVE('',#1432,#1433,#1022,.T.);
#1759=EDGE_CURVE('',#1433,#1433,#385,.T.);
#1760=EDGE_CURVE('',#1434,#1432,#149,.T.);
#1761=EDGE_CURVE('',#1435,#1434,#150,.T.);
#1762=EDGE_CURVE('',#1436,#1435,#151,.T.);
#1763=EDGE_CURVE('',#1431,#1436,#152,.T.);
#1764=EDGE_CURVE('',#1437,#1437,#386,.T.);
#1765=EDGE_CURVE('',#1437,#1438,#1023,.T.);
#1766=EDGE_CURVE('',#1439,#1438,#153,.T.);
#1767=EDGE_CURVE('',#1440,#1439,#154,.T.);
#1768=EDGE_CURVE('',#1441,#1440,#155,.T.);
#1769=EDGE_CURVE('',#1442,#1441,#156,.T.);
#1770=EDGE_CURVE('',#1443,#1442,#157,.T.);
#1771=EDGE_CURVE('',#1438,#1443,#158,.T.);
#1772=EDGE_CURVE('',#1434,#1443,#1024,.T.);
#1773=EDGE_CURVE('',#1435,#1442,#1025,.T.);
#1774=EDGE_CURVE('',#1432,#1438,#1026,.T.);
#1775=EDGE_CURVE('',#1430,#1439,#1027,.T.);
#1776=EDGE_CURVE('',#1444,#1444,#387,.F.);
#1777=EDGE_CURVE('',#1444,#1445,#1028,.T.);
#1778=EDGE_CURVE('',#1445,#1445,#388,.F.);
#1779=EDGE_CURVE('',#1431,#1440,#1029,.T.);
#1780=EDGE_CURVE('',#1436,#1441,#1030,.T.);
#2332=ORIENTED_EDGE('',*,*,#1756,.F.);
#2333=ORIENTED_EDGE('',*,*,#1757,.F.);
#2334=ORIENTED_EDGE('',*,*,#1758,.T.);
#2335=ORIENTED_EDGE('',*,*,#1759,.F.);
#2336=ORIENTED_EDGE('',*,*,#1758,.F.);
#2337=ORIENTED_EDGE('',*,*,#1760,.F.);
#2338=ORIENTED_EDGE('',*,*,#1761,.F.);
#2339=ORIENTED_EDGE('',*,*,#1762,.F.);
#2340=ORIENTED_EDGE('',*,*,#1763,.F.);
#2341=ORIENTED_EDGE('',*,*,#1764,.F.);
#2342=ORIENTED_EDGE('',*,*,#1765,.T.);
#2343=ORIENTED_EDGE('',*,*,#1766,.F.);
#2344=ORIENTED_EDGE('',*,*,#1767,.F.);
#2345=ORIENTED_EDGE('',*,*,#1768,.F.);
#2346=ORIENTED_EDGE('',*,*,#1769,.F.);
#2347=ORIENTED_EDGE('',*,*,#1770,.F.);
#2348=ORIENTED_EDGE('',*,*,#1771,.F.);
#2349=ORIENTED_EDGE('',*,*,#1765,.F.);
#2350=ORIENTED_EDGE('',*,*,#1761,.T.);
#2351=ORIENTED_EDGE('',*,*,#1772,.T.);
#2352=ORIENTED_EDGE('',*,*,#1770,.T.);
#2353=ORIENTED_EDGE('',*,*,#1773,.F.);
#2354=ORIENTED_EDGE('',*,*,#1760,.T.);
#2355=ORIENTED_EDGE('',*,*,#1774,.T.);
#2356=ORIENTED_EDGE('',*,*,#1771,.T.);
#2357=ORIENTED_EDGE('',*,*,#1772,.F.);
#2358=ORIENTED_EDGE('',*,*,#1757,.T.);
#2359=ORIENTED_EDGE('',*,*,#1775,.T.);
#2360=ORIENTED_EDGE('',*,*,#1766,.T.);
#2361=ORIENTED_EDGE('',*,*,#1774,.F.);
#2362=ORIENTED_EDGE('',*,*,#1776,.F.);
#2363=ORIENTED_EDGE('',*,*,#1777,.T.);
#2364=ORIENTED_EDGE('',*,*,#1778,.T.);
#2365=ORIENTED_EDGE('',*,*,#1777,.F.);
#2366=ORIENTED_EDGE('',*,*,#1756,.T.);
#2367=ORIENTED_EDGE('',*,*,#1779,.T.);
#2368=ORIENTED_EDGE('',*,*,#1767,.T.);
#2369=ORIENTED_EDGE('',*,*,#1775,.F.);
#2370=ORIENTED_EDGE('',*,*,#1762,.T.);
#2371=ORIENTED_EDGE('',*,*,#1773,.T.);
#2372=ORIENTED_EDGE('',*,*,#1769,.T.);
#2373=ORIENTED_EDGE('',*,*,#1780,.F.);
#2374=ORIENTED_EDGE('',*,*,#1763,.T.);
#2375=ORIENTED_EDGE('',*,*,#1780,.T.);
#2376=ORIENTED_EDGE('',*,*,#1768,.T.);
#2377=ORIENTED_EDGE('',*,*,#1779,.F.);
#2378=ORIENTED_EDGE('',*,*,#1764,.T.);
#2379=ORIENTED_EDGE('',*,*,#1776,.T.);
#2380=ORIENTED_EDGE('',*,*,#1759,.T.);
#2381=ORIENTED_EDGE('',*,*,#1778,.F.);
#2764=PLANE('',#3348);
#2765=PLANE('',#3349);
#2766=PLANE('',#3350);
#2767=PLANE('',#3354);
#2768=PLANE('',#3355);
#2769=PLANE('',#3356);
#2770=PLANE('',#3357);
#2771=PLANE('',#3358);
#2898=ADVANCED_FACE('',(#565),#164,.T.);
#2899=ADVANCED_FACE('',(#566),#165,.T.);
#2900=ADVANCED_FACE('',(#567),#2764,.T.);
#2901=ADVANCED_FACE('',(#568),#2765,.T.);
#2902=ADVANCED_FACE('',(#569),#2766,.T.);
#2903=ADVANCED_FACE('',(#570),#273,.F.);
#2904=ADVANCED_FACE('',(#571),#2767,.T.);
#2905=ADVANCED_FACE('',(#572),#2768,.T.);
#2906=ADVANCED_FACE('',(#573),#2769,.T.);
#2907=ADVANCED_FACE('',(#574,#321),#2770,.T.);
#2908=ADVANCED_FACE('',(#575,#322),#2771,.F.);
#2995=CLOSED_SHELL('',(#2898,#2899,#2900,#2901,#2902,#2903,#2904,#2905,
#2906,#2907,#2908));
#3343=AXIS2_PLACEMENT_3D('',#4930,#3992,#3993);
#3344=AXIS2_PLACEMENT_3D('',#4931,#3994,#3995);
#3345=AXIS2_PLACEMENT_3D('',#4943,#3997,#3998);
#3346=AXIS2_PLACEMENT_3D('',#4959,#3999,#4000);
#3347=AXIS2_PLACEMENT_3D('',#4961,#4001,#4002);
#3348=AXIS2_PLACEMENT_3D('',#4987,#4004,#4005);
#3349=AXIS2_PLACEMENT_3D('',#4990,#4008,#4009);
#3350=AXIS2_PLACEMENT_3D('',#4992,#4011,#4012);
#3351=AXIS2_PLACEMENT_3D('',#4994,#4014,#4015);
#3352=AXIS2_PLACEMENT_3D('',#4996,#4016,#4017);
#3353=AXIS2_PLACEMENT_3D('',#4999,#4019,#4020);
#3354=AXIS2_PLACEMENT_3D('',#5000,#4021,#4022);
#3355=AXIS2_PLACEMENT_3D('',#5002,#4024,#4025);
#3356=AXIS2_PLACEMENT_3D('',#5004,#4027,#4028);
#3357=AXIS2_PLACEMENT_3D('',#5005,#4029,#4030);
#3358=AXIS2_PLACEMENT_3D('',#5006,#4031,#4032);
#3992=DIRECTION('axis',(0.,0.,1.));
#3993=DIRECTION('refdir',(1.,0.,0.));
#3994=DIRECTION('center_axis',(0.,1.,0.));
#3995=DIRECTION('ref_axis',(1.,0.,0.));
#3996=DIRECTION('',(0.866025403784439,-0.5,1.06057523872491E-16));
#3997=DIRECTION('center_axis',(0.,-1.,0.));
#3998=DIRECTION('ref_axis',(1.,0.,0.));
#3999=DIRECTION('center_axis',(0.,-1.,0.));
#4000=DIRECTION('ref_axis',(1.,0.,0.));
#4001=DIRECTION('center_axis',(0.,1.,0.));
#4002=DIRECTION('ref_axis',(1.,0.,0.));
#4003=DIRECTION('',(-0.866025403784439,-0.5,-1.06057523872491E-16));
#4004=DIRECTION('center_axis',(1.92296268638356E-16,0.,-1.));
#4005=DIRECTION('ref_axis',(-1.,0.,-1.92296268638356E-16));
#4006=DIRECTION('',(0.,1.,0.));
#4007=DIRECTION('',(0.,1.,0.));
#4008=DIRECTION('center_axis',(-0.866025403784439,0.,-0.5));
#4009=DIRECTION('ref_axis',(-0.5,0.,0.866025403784439));
#4010=DIRECTION('',(0.,1.,0.));
#4011=DIRECTION('center_axis',(-0.866025403784439,0.,0.5));
#4012=DIRECTION('ref_axis',(0.5,0.,0.866025403784439));
#4013=DIRECTION('',(0.,1.,0.));
#4014=DIRECTION('center_axis',(0.,1.,0.));
#4015=DIRECTION('ref_axis',(1.,0.,0.));
#4016=DIRECTION('center_axis',(0.,1.,0.));
#4017=DIRECTION('ref_axis',(1.,0.,0.));
#4018=DIRECTION('',(0.,-1.,0.));
#4019=DIRECTION('center_axis',(0.,1.,0.));
#4020=DIRECTION('ref_axis',(1.,0.,0.));
#4021=DIRECTION('center_axis',(-1.92296268638356E-16,0.,1.));
#4022=DIRECTION('ref_axis',(1.,0.,1.92296268638356E-16));
#4023=DIRECTION('',(0.,1.,0.));
#4024=DIRECTION('center_axis',(0.866025403784439,0.,-0.5));
#4025=DIRECTION('ref_axis',(-0.5,0.,-0.866025403784439));
#4026=DIRECTION('',(0.,1.,0.));
#4027=DIRECTION('center_axis',(0.866025403784439,0.,0.5));
#4028=DIRECTION('ref_axis',(0.5,0.,-0.866025403784439));
#4029=DIRECTION('center_axis',(0.,1.,0.));
#4030=DIRECTION('ref_axis',(1.,0.,0.));
#4031=DIRECTION('center_axis',(0.,1.,0.));
#4032=DIRECTION('ref_axis',(1.,0.,0.));
#4930=CARTESIAN_POINT('',(0.,0.,0.));
#4931=CARTESIAN_POINT('Origin',(0.,0.0584134911936118,0.));
#4932=CARTESIAN_POINT('',(-0.288675134594813,0.0590919554682611,0.5));
#4933=CARTESIAN_POINT('',(0.288675134594813,0.0590919554682611,0.5));
#4934=CARTESIAN_POINT('Ctrl Pts',(-0.288675134594813,0.0590919554682611,
0.5));
#4935=CARTESIAN_POINT('Ctrl Pts',(2.1664336991023E-12,-0.0242413778636964,
0.5));
#4936=CARTESIAN_POINT('Ctrl Pts',(0.288675134594813,0.0590919554682611,
0.5));
#4937=CARTESIAN_POINT('',(-0.577350269189626,0.0590919554682611,-7.07050159149938E-17));
#4938=CARTESIAN_POINT('Ctrl Pts',(-0.577350269189626,0.0590919554682611,
-7.07050159149938E-17));
#4939=CARTESIAN_POINT('Ctrl Pts',(-0.433012701891136,-0.0242413778636963,
0.250000000001876));
#4940=CARTESIAN_POINT('Ctrl Pts',(-0.288675134594813,0.0590919554682611,
0.5));
#4941=CARTESIAN_POINT('',(-0.475,-4.16333634234434E-17,-5.81707229594993E-17));
#4942=CARTESIAN_POINT('',(-0.576175134594813,0.0584134911936118,-7.05611034329833E-17));
#4943=CARTESIAN_POINT('Origin',(0.,0.,0.));
#4944=CARTESIAN_POINT('',(-0.288675134594813,0.0590919554682611,-0.5));
#4945=CARTESIAN_POINT('Ctrl Pts',(-0.288675134594813,0.0590919554682611,
-0.5));
#4946=CARTESIAN_POINT('Ctrl Pts',(-0.433012701893303,-0.0242413778636963,
-0.249999999998124));
#4947=CARTESIAN_POINT('Ctrl Pts',(-0.577350269189626,0.0590919554682611,
-7.07050159149938E-17));
#4948=CARTESIAN_POINT('',(0.288675134594813,0.0590919554682611,-0.5));
#4949=CARTESIAN_POINT('Ctrl Pts',(0.288675134594813,0.0590919554682611,
-0.5));
#4950=CARTESIAN_POINT('Ctrl Pts',(-2.16648921025353E-12,-0.0242413778636962,
-0.5));
#4951=CARTESIAN_POINT('Ctrl Pts',(-0.288675134594813,0.0590919554682611,
-0.5));
#4952=CARTESIAN_POINT('',(0.577350269189626,0.0590919554682611,0.));
#4953=CARTESIAN_POINT('Ctrl Pts',(0.577350269189626,0.0590919554682611,
0.));
#4954=CARTESIAN_POINT('Ctrl Pts',(0.433012701891136,-0.0242413778636963,
-0.250000000001876));
#4955=CARTESIAN_POINT('Ctrl Pts',(0.288675134594813,0.0590919554682611,
-0.5));
#4956=CARTESIAN_POINT('Ctrl Pts',(0.288675134594813,0.0590919554682611,
0.5));
#4957=CARTESIAN_POINT('Ctrl Pts',(0.433012701893303,-0.0242413778636962,
0.249999999998124));
#4958=CARTESIAN_POINT('Ctrl Pts',(0.577350269189626,0.0590919554682611,
0.));
#4959=CARTESIAN_POINT('Origin',(0.,0.461586508806388,0.));
#4960=CARTESIAN_POINT('',(-0.475,0.52,-5.81707229594993E-17));
#4961=CARTESIAN_POINT('Origin',(0.,0.52,0.));
#4962=CARTESIAN_POINT('',(-0.577350269189626,0.460908044531739,-7.07050159149938E-17));
#4963=CARTESIAN_POINT('',(-0.576175134594813,0.461586508806388,-7.05611034329833E-17));
#4964=CARTESIAN_POINT('',(-0.288675134594813,0.460908044531739,0.5));
#4965=CARTESIAN_POINT('Ctrl Pts',(-0.288675134594813,0.460908044531739,
0.5));
#4966=CARTESIAN_POINT('Ctrl Pts',(-0.433012701893303,0.544241377863696,
0.249999999998124));
#4967=CARTESIAN_POINT('Ctrl Pts',(-0.577350269189626,0.460908044531739,
-7.07050159149938E-17));
#4968=CARTESIAN_POINT('',(0.288675134594813,0.460908044531739,0.5));
#4969=CARTESIAN_POINT('Ctrl Pts',(0.288675134594813,0.460908044531739,0.5));
#4970=CARTESIAN_POINT('Ctrl Pts',(-2.16676676600969E-12,0.544241377863697,
0.5));
#4971=CARTESIAN_POINT('Ctrl Pts',(-0.288675134594813,0.460908044531739,
0.5));
#4972=CARTESIAN_POINT('',(0.577350269189626,0.460908044531739,0.));
#4973=CARTESIAN_POINT('Ctrl Pts',(0.577350269189626,0.460908044531739,0.));
#4974=CARTESIAN_POINT('Ctrl Pts',(0.433012701891136,0.544241377863696,0.250000000001876));
#4975=CARTESIAN_POINT('Ctrl Pts',(0.288675134594813,0.460908044531739,0.5));
#4976=CARTESIAN_POINT('',(0.288675134594813,0.460908044531739,-0.5));
#4977=CARTESIAN_POINT('Ctrl Pts',(0.288675134594813,0.460908044531739,-0.5));
#4978=CARTESIAN_POINT('Ctrl Pts',(0.433012701893302,0.544241377863696,-0.249999999998124));
#4979=CARTESIAN_POINT('Ctrl Pts',(0.577350269189626,0.460908044531739,0.));
#4980=CARTESIAN_POINT('',(-0.288675134594813,0.460908044531739,-0.5));
#4981=CARTESIAN_POINT('Ctrl Pts',(-0.288675134594813,0.460908044531739,
-0.5));
#4982=CARTESIAN_POINT('Ctrl Pts',(2.16660023255599E-12,0.544241377863697,
-0.5));
#4983=CARTESIAN_POINT('Ctrl Pts',(0.288675134594813,0.460908044531739,-0.5));
#4984=CARTESIAN_POINT('Ctrl Pts',(-0.577350269189626,0.460908044531739,
-7.07050159149938E-17));
#4985=CARTESIAN_POINT('Ctrl Pts',(-0.433012701891136,0.544241377863696,
-0.250000000001876));
#4986=CARTESIAN_POINT('Ctrl Pts',(-0.288675134594813,0.460908044531739,
-0.5));
#4987=CARTESIAN_POINT('Origin',(0.288675134594813,0.,-0.5));
#4988=CARTESIAN_POINT('',(-0.288675134594813,0.,-0.5));
#4989=CARTESIAN_POINT('',(0.288675134594813,0.,-0.5));
#4990=CARTESIAN_POINT('Origin',(-0.288675134594813,0.,-0.5));
#4991=CARTESIAN_POINT('',(-0.577350269189626,0.,-7.07050159149938E-17));
#4992=CARTESIAN_POINT('Origin',(-0.577350269189626,0.,-7.07050159149938E-17));
#4993=CARTESIAN_POINT('',(-0.288675134594813,0.,0.5));
#4994=CARTESIAN_POINT('Origin',(0.,0.,0.));
#4995=CARTESIAN_POINT('',(-0.25175,0.52,3.08304831685346E-17));
#4996=CARTESIAN_POINT('Origin',(0.,0.52,0.));
#4997=CARTESIAN_POINT('',(-0.25175,0.,3.08304831685346E-17));
#4998=CARTESIAN_POINT('',(-0.25175,0.,3.08304831685346E-17));
#4999=CARTESIAN_POINT('Origin',(0.,0.,0.));
#5000=CARTESIAN_POINT('Origin',(-0.288675134594813,0.,0.5));
#5001=CARTESIAN_POINT('',(0.288675134594813,0.,0.5));
#5002=CARTESIAN_POINT('Origin',(0.577350269189626,0.,0.));
#5003=CARTESIAN_POINT('',(0.577350269189626,0.,0.));
#5004=CARTESIAN_POINT('Origin',(0.288675134594813,0.,0.5));
#5005=CARTESIAN_POINT('Origin',(0.,0.52,0.));
#5006=CARTESIAN_POINT('Origin',(0.,0.,0.));
#5698=UNCERTAINTY_MEASURE_WITH_UNIT(LENGTH_MEASURE(0.001),#5735,
'DISTANCE_ACCURACY_VALUE',
'Maximum model space distance between geometric entities at asserted c
onnectivities');
#5711=UNCERTAINTY_MEASURE_WITH_UNIT(LENGTH_MEASURE(0.001),#5735,
'DISTANCE_ACCURACY_VALUE',
'Maximum model space distance between geometric entities at asserted c
onnectivities');
#5721=(
GEOMETRIC_REPRESENTATION_CONTEXT(3)
GLOBAL_UNCERTAINTY_ASSIGNED_CONTEXT((#5698))
GLOBAL_UNIT_ASSIGNED_CONTEXT((#5735,#5737,#5738))
REPRESENTATION_CONTEXT('','3D')
);
#5734=(
GEOMETRIC_REPRESENTATION_CONTEXT(3)
GLOBAL_UNCERTAINTY_ASSIGNED_CONTEXT((#5711))
GLOBAL_UNIT_ASSIGNED_CONTEXT((#5735,#5737,#5738))
REPRESENTATION_CONTEXT('','3D')
);
#5735=(
LENGTH_UNIT()
NAMED_UNIT(*)
SI_UNIT(.CENTI.,.METRE.)
);
#5737=(
NAMED_UNIT(*)
PLANE_ANGLE_UNIT()
SI_UNIT($,.RADIAN.)
);
#5738=(
NAMED_UNIT(*)
SI_UNIT($,.STERADIAN.)
SOLID_ANGLE_UNIT()
);
#5748=SHAPE_DEFINITION_REPRESENTATION(#5770,#5817);
#5770=PRODUCT_DEFINITION_SHAPE('',$,#5840);
#5817=SHAPE_REPRESENTATION('',(#3343),#5721);
#5830=PRODUCT_DEFINITION_CONTEXT('part definition',#5898,'design');
#5840=PRODUCT_DEFINITION('Hex Nut - M6','Hex Nut - M6',#5862,#5830);
#5862=PRODUCT_DEFINITION_FORMATION('',$,#5909);
#5898=APPLICATION_CONTEXT(
'Core Data for Automotive Mechanical Design Process');
#5899=PRODUCT_CONTEXT('part definition',#5898,'mechanical');
#5909=PRODUCT('Hex Nut - M6','Hex Nut - M6','Hex Nut - M6',(#5899));
#5985=COLOUR_RGB('Black',0.12,0.14,0.17);
#5986=FILL_AREA_STYLE_COLOUR('',#5985);
#5987=FILL_AREA_STYLE('',(#5986));
#5988=SURFACE_STYLE_FILL_AREA(#5987);
#5989=SURFACE_SIDE_STYLE('',(#5988));
#5990=SURFACE_STYLE_USAGE(.BOTH.,#5989);
#5991=PRESENTATION_STYLE_ASSIGNMENT((#5990));
ENDSEC;
END-ISO-10303-21;
